ISO-10303-21;
HEADER;
/* Generated by software containing ST-Developer
 * from STEP Tools, Inc. (www.steptools.com) 
 */

FILE_DESCRIPTION(
/* description */ ('Lifting hook block with sheave'),
/* implementation_level */ '2;1');

FILE_NAME(
/* name */ 'Hex Nut - M8.step',
/* time_stamp */ '2026-10-28T03:23:54-07:00',
/* author */ (''),
/* organization */ (''),
/* preprocessor_version */ 'ST-DEVELOPER v20.2',
/* originating_system */ 'Autodesk Translation Framework v15.17.0.0',
/* authorisation */ '');

FILE_SCHEMA (('AUTOMOTIVE_DESIGN { 1 0 10303 214 3 1 1 }'));
ENDSEC;

DATA;
#10=MECHANICAL_DESIGN_GEOMETRIC_PRESENTATION_REPRESENTATION('',(#365),#9391);
#255=(
BOUNDED_CURVE()
B_SPLINE_CURVE(2,(#8141,#8142,#8143),.UNSPECIFIED.,.F.,.F.)
B_SPLINE_CURVE_WITH_KNOTS((3,3),(0.14973948338295,0.97160236658079),
 .UNSPECIFIED.)
CURVE()
GEOMETRIC_REPRESENTATION_ITEM()
RATIONAL_B_SPLINE_CURVE((1.07140024848292,1.23714644374248,1.07140024848292))
REPRESENTATION_ITEM('')
);
#256=(
BOUNDED_CURVE()
B_SPLINE_CURVE(2,(#8145,#8146,#8147),.UNSPECIFIED.,.F.,.F.)
B_SPLINE_CURVE_WITH_KNOTS((3,3),(0.14973948338295,0.971602366580789),
 .UNSPECIFIED.)
CURVE()
GEOMETRIC_REPRESENTATION_ITEM()
RATIONAL_B_SPLINE_CURVE((1.07140024848292,1.23714644374248,1.07140024848292))
REPRESENTATION_ITEM('')
);
#257=(
BOUNDED_CURVE()
B_SPLINE_CURVE(2,(#8152,#8153,#8154),.UNSPECIFIED.,.F.,.F.)
B_SPLINE_CURVE_WITH_KNOTS((3,3),(0.14973948338295,0.97160236658079),
 .UNSPECIFIED.)
CURVE()
GEOMETRIC_REPRESENTATION_ITEM()
RATIONAL_B_SPLINE_CURVE((1.07140024848292,1.23714644374248,1.07140024848292))
REPRESENTATION_ITEM('')
);
#258=(
BOUNDED_CURVE()
B_SPLINE_CURVE(2,(#8156,#8157,#8158),.UNSPECIFIED.,.F.,.F.)
B_SPLINE_CURVE_WITH_KNOTS((3,3),(0.14973948338295,0.97160236658079),
 .UNSPECIFIED.)
CURVE()
GEOMETRIC_REPRESENTATION_ITEM()
RATIONAL_B_SPLINE_CURVE((1.07140024848292,1.23714644374248,1.07140024848292))
REPRESENTATION_ITEM('')
);
#259=(
BOUNDED_CURVE()
B_SPLINE_CURVE(2,(#8160,#8161,#8162),.UNSPECIFIED.,.F.,.F.)
B_SPLINE_CURVE_WITH_KNOTS((3,3),(0.14973948338295,0.971602366580789),
 .UNSPECIFIED.)
CURVE()
GEOMETRIC_REPRESENTATION_ITEM()
RATIONAL_B_SPLINE_CURVE((1.07140024848292,1.23714644374248,1.07140024848292))
REPRESENTATION_ITEM('')
);
#260=(
BOUNDED_CURVE()
B_SPLINE_CURVE(2,(#8163,#8164,#8165),.UNSPECIFIED.,.F.,.F.)
B_SPLINE_CURVE_WITH_KNOTS((3,3),(0.14973948338295,0.97160236658079),
 .UNSPECIFIED.)
CURVE()
GEOMETRIC_REPRESENTATION_ITEM()
RATIONAL_B_SPLINE_CURVE((1.07140024848292,1.23714644374248,1.07140024848292))
REPRESENTATION_ITEM('')
);
#261=(
BOUNDED_CURVE()
B_SPLINE_CURVE(2,(#8172,#8173,#8174),.UNSPECIFIED.,.F.,.F.)
B_SPLINE_CURVE_WITH_KNOTS((3,3),(0.14973948338295,0.97160236658079),
 .UNSPECIFIED.)
CURVE()
GEOMETRIC_REPRESENTATION_ITEM()
RATIONAL_B_SPLINE_CURVE((1.07140024848292,1.23714644374248,1.07140024848292))
REPRESENTATION_ITEM('')
);
#262=(
BOUNDED_CURVE()
B_SPLINE_CURVE(2,(#8176,#8177,#8178),.UNSPECIFIED.,.F.,.F.)
B_SPLINE_CURVE_WITH_KNOTS((3,3),(0.14973948338295,0.97160236658079),
 .UNSPECIFIED.)
CURVE()
GEOMETRIC_REPRESENTATION_ITEM()
RATIONAL_B_SPLINE_CURVE((1.07140024848292,1.23714644374248,1.07140024848292))
REPRESENTATION_ITEM('')
);
#263=(
BOUNDED_CURVE()
B_SPLINE_CURVE(2,(#8180,#8181,#8182),.UNSPECIFIED.,.F.,.F.)
B_SPLINE_CURVE_WITH_KNOTS((3,3),(0.14973948338295,0.971602366580789),
 .UNSPECIFIED.)
CURVE()
GEOMETRIC_REPRESENTATION_ITEM()
RATIONAL_B_SPLINE_CURVE((1.07140024848292,1.23714644374248,1.07140024848292))
REPRESENTATION_ITEM('')
);
#264=(
BOUNDED_CURVE()
B_SPLINE_CURVE(2,(#8184,#8185,#8186),.UNSPECIFIED.,.F.,.F.)
B_SPLINE_CURVE_WITH_KNOTS((3,3),(0.14973948338295,0.97160236658079),
 .UNSPECIFIED.)
CURVE()
GEOMETRIC_REPRESENTATION_ITEM()
RATIONAL_B_SPLINE_CURVE((1.07140024848292,1.23714644374248,1.07140024848292))
REPRESENTATION_ITEM('')
);
#265=(
BOUNDED_CURVE()
B_SPLINE_CURVE(2,(#8188,#8189,#8190),.UNSPECIFIED.,.F.,.F.)
B_SPLINE_CURVE_WITH_KNOTS((3,3),(0.14973948338295,0.97160236658079),
 .UNSPECIFIED.)
CURVE()
GEOMETRIC_REPRESENTATION_ITEM()
RATIONAL_B_SPLINE_CURVE((1.07140024848292,1.23714644374248,1.07140024848292))
REPRESENTATION_ITEM('')
);
#266=(
BOUNDED_CURVE()
B_SPLINE_CURVE(2,(#8191,#8192,#8193),.UNSPECIFIED.,.F.,.F.)
B_SPLINE_CURVE_WITH_KNOTS((3,3),(0.14973948338295,0.971602366580789),
 .UNSPECIFIED.)
CURVE()
GEOMETRIC_REPRESENTATION_ITEM()
RATIONAL_B_SPLINE_CURVE((1.07140024848292,1.23714644374248,1.07140024848292))
REPRESENTATION_ITEM('')
);
#270=CONICAL_SURFACE('',#5521,0.734027674973257,1.0471975511966);
#271=CONICAL_SURFACE('',#5523,0.734027674973257,1.0471975511966);
#305=SHAPE_REPRESENTATION_RELATIONSHIP('SRR','None',#9536,#335);
#335=ADVANCED_BREP_SHAPE_REPRESENTATION('',(#402),#9371);
#365=STYLED_ITEM('',(#9766),#402);
#402=MANIFOLD_SOLID_BREP('Body1',#4902);
#566=LINE('',#8149,#854);
#567=LINE('',#8170,#855);
#568=LINE('',#8195,#856);
#569=LINE('',#8196,#857);
#570=LINE('',#8198,#858);
#571=LINE('',#8200,#859);
#572=LINE('',#8205,#860);
#573=LINE('',#8208,#861);
#574=LINE('',#8210,#862);
#854=VECTOR('',#6597,0.734027674973257);
#855=VECTOR('',#6604,0.734027674973257);
#856=VECTOR('',#6607,1.);
#857=VECTOR('',#6608,1.);
#858=VECTOR('',#6611,1.);
#859=VECTOR('',#6614,1.);
#860=VECTOR('',#6619,0.4);
#861=VECTOR('',#6624,1.);
#862=VECTOR('',#6627,1.);
#1053=CYLINDRICAL_SURFACE('',#5528,0.338975);
#1163=FACE_BOUND('',#1697,.T.);
#1164=FACE_BOUND('',#1699,.T.);
#1342=FACE_OUTER_BOUND('',#1687,.T.);
#1343=FACE_OUTER_BOUND('',#1688,.T.);
#1344=FACE_OUTER_BOUND('',#1689,.T.);
#1345=FACE_OUTER_BOUND('',#1690,.T.);
#1346=FACE_OUTER_BOUND('',#1691,.T.);
#1347=FACE_OUTER_BOUND('',#1692,.T.);
#1348=FACE_OUTER_BOUND('',#1693,.T.);
#1349=FACE_OUTER_BOUND('',#1694,.T.);
#1350=FACE_OUTER_BOUND('',#1695,.T.);
#1351=FACE_OUTER_BOUND('',#1696,.T.);
#1352=FACE_OUTER_BOUND('',#1698,.T.);
#1687=EDGE_LOOP('',(#3764,#3765,#3766,#3767,#3768,#3769,#3770,#3771,#3772));
#1688=EDGE_LOOP('',(#3773,#3774,#3775,#3776,#3777,#3778,#3779,#3780,#3781));
#1689=EDGE_LOOP('',(#3782,#3783,#3784,#3785));
#1690=EDGE_LOOP('',(#3786,#3787,#3788,#3789));
#1691=EDGE_LOOP('',(#3790,#3791,#3792,#3793));
#1692=EDGE_LOOP('',(#3794,#3795,#3796,#3797));
#1693=EDGE_LOOP('',(#3798,#3799,#3800,#3801));
#1694=EDGE_LOOP('',(#3802,#3803,#3804,#3805));
#1695=EDGE_LOOP('',(#3806,#3807,#3808,#3809));
#1696=EDGE_LOOP('',(#3810));
#1697=EDGE_LOOP('',(#3811));
#1698=EDGE_LOOP('',(#3812));
#1699=EDGE_LOOP('',(#3813));
#2040=CIRCLE('',#5522,0.6175);
#2041=CIRCLE('',#5524,0.6175);
#2042=CIRCLE('',#5529,0.338975);
#2043=CIRCLE('',#5530,0.338975);
#2385=VERTEX_POINT('',#8139);
#2386=VERTEX_POINT('',#8140);
#2387=VERTEX_POINT('',#8144);
#2388=VERTEX_POINT('',#8148);
#2389=VERTEX_POINT('',#8151);
#2390=VERTEX_POINT('',#8155);
#2391=VERTEX_POINT('',#8159);
#2392=VERTEX_POINT('',#8167);
#2393=VERTEX_POINT('',#8169);
#2394=VERTEX_POINT('',#8171);
#2395=VERTEX_POINT('',#8175);
#2396=VERTEX_POINT('',#8179);
#2397=VERTEX_POINT('',#8183);
#2398=VERTEX_POINT('',#8187);
#2399=VERTEX_POINT('',#8202);
#2400=VERTEX_POINT('',#8204);
#2886=EDGE_CURVE('',#2385,#2386,#255,.T.);
#2887=EDGE_CURVE('',#2387,#2385,#256,.T.);
#2888=EDGE_CURVE('',#2387,#2388,#566,.T.);
#2889=EDGE_CURVE('',#2388,#2388,#2040,.T.);
#2890=EDGE_CURVE('',#2389,#2387,#257,.T.);
#2891=EDGE_CURVE('',#2390,#2389,#258,.T.);
#2892=EDGE_CURVE('',#2391,#2390,#259,.T.);
#2893=EDGE_CURVE('',#2386,#2391,#260,.T.);
#2894=EDGE_CURVE('',#2392,#2392,#2041,.T.);
#2895=EDGE_CURVE('',#2392,#2393,#567,.T.);
#2896=EDGE_CURVE('',#2394,#2393,#261,.T.);
#2897=EDGE_CURVE('',#2395,#2394,#262,.T.);
#2898=EDGE_CURVE('',#2396,#2395,#263,.T.);
#2899=EDGE_CURVE('',#2397,#2396,#264,.T.);
#2900=EDGE_CURVE('',#2398,#2397,#265,.T.);
#2901=EDGE_CURVE('',#2393,#2398,#266,.T.);
#2902=EDGE_CURVE('',#2389,#2398,#568,.T.);
#2903=EDGE_CURVE('',#2390,#2397,#569,.T.);
#2904=EDGE_CURVE('',#2387,#2393,#570,.T.);
#2905=EDGE_CURVE('',#2385,#2394,#571,.T.);
#2906=EDGE_CURVE('',#2399,#2399,#2042,.F.);
#2907=EDGE_CURVE('',#2399,#2400,#572,.T.);
#2908=EDGE_CURVE('',#2400,#2400,#2043,.F.);
#2909=EDGE_CURVE('',#2386,#2395,#573,.T.);
#2910=EDGE_CURVE('',#2391,#2396,#574,.T.);
#3764=ORIENTED_EDGE('',*,*,#2886,.F.);
#3765=ORIENTED_EDGE('',*,*,#2887,.F.);
#3766=ORIENTED_EDGE('',*,*,#2888,.T.);
#3767=ORIENTED_EDGE('',*,*,#2889,.F.);
#3768=ORIENTED_EDGE('',*,*,#2888,.F.);
#3769=ORIENTED_EDGE('',*,*,#2890,.F.);
#3770=ORIENTED_EDGE('',*,*,#2891,.F.);
#3771=ORIENTED_EDGE('',*,*,#2892,.F.);
#3772=ORIENTED_EDGE('',*,*,#2893,.F.);
#3773=ORIENTED_EDGE('',*,*,#2894,.F.);
#3774=ORIENTED_EDGE('',*,*,#2895,.T.);
#3775=ORIENTED_EDGE('',*,*,#2896,.F.);
#3776=ORIENTED_EDGE('',*,*,#2897,.F.);
#3777=ORIENTED_EDGE('',*,*,#2898,.F.);
#3778=ORIENTED_EDGE('',*,*,#2899,.F.);
#3779=ORIENTED_EDGE('',*,*,#2900,.F.);
#3780=ORIENTED_EDGE('',*,*,#2901,.F.);
#3781=ORIENTED_EDGE('',*,*,#2895,.F.);
#3782=ORIENTED_EDGE('',*,*,#2891,.T.);
#3783=ORIENTED_EDGE('',*,*,#2902,.T.);
#3784=ORIENTED_EDGE('',*,*,#2900,.T.);
#3785=ORIENTED_EDGE('',*,*,#2903,.F.);
#3786=ORIENTED_EDGE('',*,*,#2890,.T.);
#3787=ORIENTED_EDGE('',*,*,#2904,.T.);
#3788=ORIENTED_EDGE('',*,*,#2901,.T.);
#3789=ORIENTED_EDGE('',*,*,#2902,.F.);
#3790=ORIENTED_EDGE('',*,*,#2887,.T.);
#3791=ORIENTED_EDGE('',*,*,#2905,.T.);
#3792=ORIENTED_EDGE('',*,*,#2896,.T.);
#3793=ORIENTED_EDGE('',*,*,#2904,.F.);
#3794=ORIENTED_EDGE('',*,*,#2906,.F.);
#3795=ORIENTED_EDGE('',*,*,#2907,.T.);
#3796=ORIENTED_EDGE('',*,*,#2908,.T.);
#3797=ORIENTED_EDGE('',*,*,#2907,.F.);
#3798=ORIENTED_EDGE('',*,*,#2886,.T.);
#3799=ORIENTED_EDGE('',*,*,#2909,.T.);
#3800=ORIENTED_EDGE('',*,*,#2897,.T.);
#3801=ORIENTED_EDGE('',*,*,#2905,.F.);
#3802=ORIENTED_EDGE('',*,*,#2892,.T.);
#3803=ORIENTED_EDGE('',*,*,#2903,.T.);
#3804=ORIENTED_EDGE('',*,*,#2899,.T.);
#3805=ORIENTED_EDGE('',*,*,#2910,.F.);
#3806=ORIENTED_EDGE('',*,*,#2893,.T.);
#3807=ORIENTED_EDGE('',*,*,#2910,.T.);
#3808=ORIENTED_EDGE('',*,*,#2898,.T.);
#3809=ORIENTED_EDGE('',*,*,#2909,.F.);
#3810=ORIENTED_EDGE('',*,*,#2894,.T.);
#3811=ORIENTED_EDGE('',*,*,#2906,.T.);
#3812=ORIENTED_EDGE('',*,*,#2889,.T.);
#3813=ORIENTED_EDGE('',*,*,#2908,.F.);
#4516=PLANE('',#5525);
#4517=PLANE('',#5526);
#4518=PLANE('',#5527);
#4519=PLANE('',#5531);
#4520=PLANE('',#5532);
#4521=PLANE('',#5533);
#4522=PLANE('',#5534);
#4523=PLANE('',#5535);
#4718=ADVANCED_FACE('',(#1342),#270,.T.);
#4719=ADVANCED_FACE('',(#1343),#271,.T.);
#4720=ADVANCED_FACE('',(#1344),#4516,.T.);
#4721=ADVANCED_FACE('',(#1345),#4517,.T.);
#4722=ADVANCED_FACE('',(#1346),#4518,.T.);
#4723=ADVANCED_FACE('',(#1347),#1053,.F.);
#4724=ADVANCED_FACE('',(#1348),#4519,.T.);
#4725=ADVANCED_FACE('',(#1349),#4520,.T.);
#4726=ADVANCED_FACE('',(#1350),#4521,.T.);
#4727=ADVANCED_FACE('',(#1351,#1163),#4522,.T.);
#4728=ADVANCED_FACE('',(#1352,#1164),#4523,.F.);
#4902=CLOSED_SHELL('',(#4718,#4719,#4720,#4721,#4722,#4723,#4724,#4725,
#4726,#4727,#4728));
#5520=AXIS2_PLACEMENT_3D('',#8137,#6593,#6594);
#5521=AXIS2_PLACEMENT_3D('',#8138,#6595,#6596);
#5522=AXIS2_PLACEMENT_3D('',#8150,#6598,#6599);
#5523=AXIS2_PLACEMENT_3D('',#8166,#6600,#6601);
#5524=AXIS2_PLACEMENT_3D('',#8168,#6602,#6603);
#5525=AXIS2_PLACEMENT_3D('',#8194,#6605,#6606);
#5526=AXIS2_PLACEMENT_3D('',#8197,#6609,#6610);
#5527=AXIS2_PLACEMENT_3D('',#8199,#6612,#6613);
#5528=AXIS2_PLACEMENT_3D('',#8201,#6615,#6616);
#5529=AXIS2_PLACEMENT_3D('',#8203,#6617,#6618);
#5530=AXIS2_PLACEMENT_3D('',#8206,#6620,#6621);
#5531=AXIS2_PLACEMENT_3D('',#8207,#6622,#6623);
#5532=AXIS2_PLACEMENT_3D('',#8209,#6625,#6626);
#5533=AXIS2_PLACEMENT_3D('',#8211,#6628,#6629);
#5534=AXIS2_PLACEMENT_3D('',#8212,#6630,#6631);
#5535=AXIS2_PLACEMENT_3D('',#8213,#6632,#6633);
#6593=DIRECTION('axis',(0.,0.,1.));
#6594=DIRECTION('refdir',(1.,0.,0.));
#6595=DIRECTION('center_axis',(0.,1.,0.));
#6596=DIRECTION('ref_axis',(1.,0.,0.));
#6597=DIRECTION('',(0.866025403784439,-0.5,1.06057523872491E-16));
#6598=DIRECTION('center_axis',(0.,-1.,0.));
#6599=DIRECTION('ref_axis',(1.,0.,0.));
#6600=DIRECTION('center_axis',(0.,-1.,0.));
#6601=DIRECTION('ref_axis',(1.,0.,0.));
#6602=DIRECTION('center_axis',(0.,1.,0.));
#6603=DIRECTION('ref_axis',(1.,0.,0.));
#6604=DIRECTION('',(-0.866025403784439,-0.5,-1.06057523872491E-16));
#6605=DIRECTION('center_axis',(1.4792020664489E-16,0.,-1.));
#6606=DIRECTION('ref_axis',(-1.,0.,-1.4792020664489E-16));
#6607=DIRECTION('',(0.,1.,0.));
#6608=DIRECTION('',(0.,1.,0.));
#6609=DIRECTION('center_axis',(-0.866025403784439,0.,-0.5));
#6610=DIRECTION('ref_axis',(-0.5,0.,0.866025403784439));
#6611=DIRECTION('',(0.,1.,0.));
#6612=DIRECTION('center_axis',(-0.866025403784439,0.,0.5));
#6613=DIRECTION('ref_axis',(0.5,0.,0.866025403784439));
#6614=DIRECTION('',(0.,1.,0.));
#6615=DIRECTION('center_axis',(0.,1.,0.));
#6616=DIRECTION('ref_axis',(1.,0.,0.));
#6617=DIRECTION('center_axis',(0.,1.,0.));
#6618=DIRECTION('ref_axis',(1.,0.,0.));
#6619=DIRECTION('',(0.,-1.,0.));
#6620=DIRECTION('center_axis',(0.,1.,0.));
#6621=DIRECTION('ref_axis',(1.,0.,0.));
#6622=DIRECTION('center_axis',(-2.95840413289779E-16,0.,1.));
#6623=DIRECTION('ref_axis',(1.,0.,2.95840413289779E-16));
#6624=DIRECTION('',(0.,1.,0.));
#6625=DIRECTION('center_axis',(0.866025403784439,0.,-0.5));
#6626=DIRECTION('ref_axis',(-0.5,0.,-0.866025403784439));
#6627=DIRECTION('',(0.,1.,0.));
#6628=DIRECTION('center_axis',(0.866025403784439,0.,0.5));
#6629=DIRECTION('ref_axis',(0.5,0.,-0.866025403784439));
#6630=DIRECTION('center_axis',(0.,1.,0.));
#6631=DIRECTION('ref_axis',(1.,0.,0.));
#6632=DIRECTION('center_axis',(0.,1.,0.));
#6633=DIRECTION('ref_axis',(1.,0.,0.));
#8137=CARTESIAN_POINT('',(0.,0.,0.));
#8138=CARTESIAN_POINT('Origin',(0.,0.067277284513851,0.));
#8139=CARTESIAN_POINT('',(-0.375277674973257,0.0768195421087395,0.65));
#8140=CARTESIAN_POINT('',(0.375277674973257,0.0768195421087395,0.65));
#8141=CARTESIAN_POINT('Ctrl Pts',(-0.375277674973257,0.0768195421087395,
0.65));
#8142=CARTESIAN_POINT('Ctrl Pts',(1.66533453693773E-13,-0.0315137912242439,
0.65));
#8143=CARTESIAN_POINT('Ctrl Pts',(0.375277674973257,0.0768195421087394,
0.65));
#8144=CARTESIAN_POINT('',(-0.750555349946514,0.0768195421087394,-9.19165206894919E-17));
#8145=CARTESIAN_POINT('Ctrl Pts',(-0.750555349946514,0.0768195421087394,
-9.19165206894919E-17));
#8146=CARTESIAN_POINT('Ctrl Pts',(-0.562916512459802,-0.0315137912242434,
0.325000000000144));
#8147=CARTESIAN_POINT('Ctrl Pts',(-0.375277674973257,0.0768195421087395,
0.65));
#8148=CARTESIAN_POINT('',(-0.6175,-2.77555756156289E-17,-7.5621939847349E-17));
#8149=CARTESIAN_POINT('',(-0.734027674973257,0.067277284513851,-8.98924642641573E-17));
#8150=CARTESIAN_POINT('Origin',(0.,0.,0.));
#8151=CARTESIAN_POINT('',(-0.375277674973257,0.0768195421087395,-0.65));
#8152=CARTESIAN_POINT('Ctrl Pts',(-0.375277674973257,0.0768195421087395,
-0.65));
#8153=CARTESIAN_POINT('Ctrl Pts',(-0.562916512459968,-0.0315137912242437,
-0.324999999999856));
#8154=CARTESIAN_POINT('Ctrl Pts',(-0.750555349946514,0.0768195421087395,
-9.19165206894919E-17));
#8155=CARTESIAN_POINT('',(0.375277674973257,0.0768195421087395,-0.65));
#8156=CARTESIAN_POINT('Ctrl Pts',(0.375277674973257,0.0768195421087395,
-0.65));
#8157=CARTESIAN_POINT('Ctrl Pts',(-1.66144875635155E-13,-0.0315137912242437,
-0.65));
#8158=CARTESIAN_POINT('Ctrl Pts',(-0.375277674973257,0.0768195421087395,
-0.65));
#8159=CARTESIAN_POINT('',(0.750555349946514,0.0768195421087394,0.));
#8160=CARTESIAN_POINT('Ctrl Pts',(0.750555349946514,0.0768195421087394,
0.));
#8161=CARTESIAN_POINT('Ctrl Pts',(0.562916512459802,-0.0315137912242436,
-0.325000000000144));
#8162=CARTESIAN_POINT('Ctrl Pts',(0.375277674973257,0.0768195421087395,
-0.65));
#8163=CARTESIAN_POINT('Ctrl Pts',(0.375277674973257,0.0768195421087394,
0.65));
#8164=CARTESIAN_POINT('Ctrl Pts',(0.562916512459968,-0.0315137912242439,
0.324999999999856));
#8165=CARTESIAN_POINT('Ctrl Pts',(0.750555349946514,0.0768195421087394,
0.));
#8166=CARTESIAN_POINT('Origin',(0.,0.612722715486149,0.));
#8167=CARTESIAN_POINT('',(-0.6175,0.68,-7.5621939847349E-17));
#8168=CARTESIAN_POINT('Origin',(0.,0.68,0.));
#8169=CARTESIAN_POINT('',(-0.750555349946514,0.603180457891261,-9.19165206894919E-17));
#8170=CARTESIAN_POINT('',(-0.734027674973257,0.612722715486149,-8.98924642641573E-17));
#8171=CARTESIAN_POINT('',(-0.375277674973257,0.603180457891261,0.65));
#8172=CARTESIAN_POINT('Ctrl Pts',(-0.375277674973257,0.603180457891261,
0.65));
#8173=CARTESIAN_POINT('Ctrl Pts',(-0.562916512459968,0.711513791224243,
0.324999999999856));
#8174=CARTESIAN_POINT('Ctrl Pts',(-0.750555349946514,0.603180457891261,
-9.19165206894919E-17));
#8175=CARTESIAN_POINT('',(0.375277674973257,0.603180457891261,0.65));
#8176=CARTESIAN_POINT('Ctrl Pts',(0.375277674973257,0.603180457891261,0.65));
#8177=CARTESIAN_POINT('Ctrl Pts',(-1.66755498298699E-13,0.711513791224244,
0.65));
#8178=CARTESIAN_POINT('Ctrl Pts',(-0.375277674973257,0.603180457891261,
0.65));
#8179=CARTESIAN_POINT('',(0.750555349946514,0.603180457891261,0.));
#8180=CARTESIAN_POINT('Ctrl Pts',(0.750555349946514,0.603180457891261,0.));
#8181=CARTESIAN_POINT('Ctrl Pts',(0.562916512459802,0.711513791224244,0.325000000000144));
#8182=CARTESIAN_POINT('Ctrl Pts',(0.375277674973257,0.603180457891261,0.65));
#8183=CARTESIAN_POINT('',(0.375277674973257,0.603180457891261,-0.65));
#8184=CARTESIAN_POINT('Ctrl Pts',(0.375277674973257,0.603180457891261,-0.65));
#8185=CARTESIAN_POINT('Ctrl Pts',(0.562916512459969,0.711513791224244,-0.324999999999856));
#8186=CARTESIAN_POINT('Ctrl Pts',(0.750555349946514,0.603180457891261,0.));
#8187=CARTESIAN_POINT('',(-0.375277674973257,0.603180457891261,-0.65));
#8188=CARTESIAN_POINT('Ctrl Pts',(-0.375277674973257,0.603180457891261,
-0.65));
#8189=CARTESIAN_POINT('Ctrl Pts',(1.66422431391311E-13,0.711513791224244,
-0.65));
#8190=CARTESIAN_POINT('Ctrl Pts',(0.375277674973257,0.603180457891261,-0.65));
#8191=CARTESIAN_POINT('Ctrl Pts',(-0.750555349946514,0.603180457891261,
-9.19165206894919E-17));
#8192=CARTESIAN_POINT('Ctrl Pts',(-0.562916512459802,0.711513791224244,
-0.325000000000144));
#8193=CARTESIAN_POINT('Ctrl Pts',(-0.375277674973257,0.603180457891261,
-0.65));
#8194=CARTESIAN_POINT('Origin',(0.375277674973257,0.,-0.65));
#8195=CARTESIAN_POINT('',(-0.375277674973257,0.,-0.65));
#8196=CARTESIAN_POINT('',(0.375277674973257,0.,-0.65));
#8197=CARTESIAN_POINT('Origin',(-0.375277674973257,0.,-0.65));
#8198=CARTESIAN_POINT('',(-0.750555349946514,0.,-9.19165206894919E-17));
#8199=CARTESIAN_POINT('Origin',(-0.750555349946514,0.,-9.19165206894919E-17));
#8200=CARTESIAN_POINT('',(-0.375277674973257,0.,0.65));
#8201=CARTESIAN_POINT('Origin',(0.,0.,0.));
#8202=CARTESIAN_POINT('',(-0.338975,0.68,4.15124648740974E-17));
#8203=CARTESIAN_POINT('Origin',(0.,0.68,0.));
#8204=CARTESIAN_POINT('',(-0.338975,0.,4.15124648740974E-17));
#8205=CARTESIAN_POINT('',(-0.338975,0.,4.15124648740974E-17));
#8206=CARTESIAN_POINT('Origin',(0.,0.,0.));
#8207=CARTESIAN_POINT('Origin',(-0.375277674973257,0.,0.65));
#8208=CARTESIAN_POINT('',(0.375277674973257,0.,0.65));
#8209=CARTESIAN_POINT('Origin',(0.750555349946514,0.,0.));
#8210=CARTESIAN_POINT('',(0.750555349946514,0.,0.));
#8211=CARTESIAN_POINT('Origin',(0.375277674973257,0.,0.65));
#8212=CARTESIAN_POINT('Origin',(0.,0.68,-1.11022302462516E-16));
#8213=CARTESIAN_POINT('Origin',(0.,0.,-1.11022302462516E-16));
#9334=UNCERTAINTY_MEASURE_WITH_UNIT(LENGTH_MEASURE(0.001),#9392,
'DISTANCE_ACCURACY_VALUE',
'Maximum model space distance between geometric entities at asserted c
onnectivities');
#9354=UNCERTAINTY_MEASURE_WITH_UNIT(LENGTH_MEASURE(0.001),#9392,
'DISTANCE_ACCURACY_VALUE',
'Maximum model space distance between geometric entities at asserted c
onnectivities');
#9371=(
GEOMETRIC_REPRESENTATION_CONTEXT(3)
GLOBAL_UNCERTAINTY_ASSIGNED_CONTEXT((#9334))
GLOBAL_UNIT_ASSIGNED_CONTEXT((#9392,#9394,#9395))
REPRESENTATION_CONTEXT('','3D')
);
#9391=(
GEOMETRIC_REPRESENTATION_CONTEXT(3)
GLOBAL_UNCERTAINTY_ASSIGNED_CONTEXT((#9354))
GLOBAL_UNIT_ASSIGNED_CONTEXT((#9392,#9394,#9395))
REPRESENTATION_CONTEXT('','3D')
);
#9392=(
LENGTH_UNIT()
NAMED_UNIT(*)
SI_UNIT(.CENTI.,.METRE.)
);
#9394=(
NAMED_UNIT(*)
PLANE_ANGLE_UNIT()
SI_UNIT($,.RADIAN.)
);
#9395=(
NAMED_UNIT(*)
SI_UNIT($,.STERADIAN.)
SOLID_ANGLE_UNIT()
);
#9412=SHAPE_DEFINITION_REPRESENTATION(#9448,#9536);
#9448=PRODUCT_DEFINITION_SHAPE('',$,#9573);
#9536=SHAPE_REPRESENTATION('',(#5520),#9371);
#9556=PRODUCT_DEFINITION_CONTEXT('part definition',#9666,'design');
#9573=PRODUCT_DEFINITION('Hex Nut - M8','Hex Nut - M8',#9609,#9556);
#9609=PRODUCT_DEFINITION_FORMATION('',$,#9684);
#9666=APPLICATION_CONTEXT(
'Core Data for Automotive Mechanical Design Process');
#9667=PRODUCT_CONTEXT('part definition',#9666,'mechanical');
#9684=PRODUCT('Hex Nut - M8','Hex Nut - M8','Hex Nut - M8',(#9667));
#9760=COLOUR_RGB('Black',0.12,0.14,0.17);
#9761=FILL_AREA_STYLE_COLOUR('',#9760);
#9762=FILL_AREA_STYLE('',(#9761));
#9763=SURFACE_STYLE_FILL_AREA(#9762);
#9764=SURFACE_SIDE_STYLE('',(#9763));
#9765=SURFACE_STYLE_USAGE(.BOTH.,#9764);
#9766=PRESENTATION_STYLE_ASSIGNMENT((#9765));
ENDSEC;
END-ISO-10303-21;
